ISO-10303-21;
HEADER;
/* Generated by software containing ST-Developer
 * from STEP Tools, Inc. (www.steptools.com) 
 */

FILE_DESCRIPTION(
/* description */ ('STEP AP214'),
/* implementation_level */ '2;1');

FILE_NAME(
/* name */ 'Low Head Cap Screw M6x25.step',
/* time_stamp */ '2026-11-15T14:49:54-08:00',
/* author */ (''),
/* organization */ (''),
/* preprocessor_version */ 'ST-DEVELOPER v20.2',
/* originating_system */ 'Autodesk Translation Framework v15.17.0.0',
/* authorisation */ '');

FILE_SCHEMA (('AUTOMOTIVE_DESIGN { 1 0 10303 214 3 1 1 }'));
ENDSEC;

DATA;
#10=MECHANICAL_DESIGN_GEOMETRIC_PRESENTATION_REPRESENTATION('',(#1128,#1129,#1130),#66721);
#578=CONICAL_SURFACE('',#28587,3.75,0.785398163397444);
#579=CONICAL_SURFACE('',#28591,1664.2794823505,1.02974425867665);
#1064=SHAPE_REPRESENTATION_RELATIONSHIP('SRR','None',#66927,#1095);
#1095=ADVANCED_BREP_SHAPE_REPRESENTATION('',(#1163,#1164,#1165),#66718);
#1128=STYLED_ITEM('',(#67095),#1163);
#1129=STYLED_ITEM('',(#67095),#1164);
#1130=STYLED_ITEM('',(#67095),#1165);
#1163=MANIFOLD_SOLID_BREP('Body1',#25694);
#1164=MANIFOLD_SOLID_BREP('Body2',#25695);
#1165=MANIFOLD_SOLID_BREP('Body3',#25696);
#1471=FACE_BOUND('',#5399,.T.);
#1472=FACE_BOUND('',#5402,.T.);
#1473=FACE_BOUND('',#5404,.T.);
#1474=FACE_BOUND('',#5420,.T.);
#1475=FACE_BOUND('',#5422,.T.);
#2229=PLANE('',#28607);
#2230=PLANE('',#28608);
#2231=PLANE('',#28609);
#2232=PLANE('',#28610);
#2233=PLANE('',#28611);
#2234=PLANE('',#28612);
#2235=PLANE('',#28613);
#2236=PLANE('',#28614);
#2237=PLANE('',#28615);
#2238=PLANE('',#28616);
#2239=PLANE('',#28617);
#2240=PLANE('',#28618);
#2241=PLANE('',#28619);
#2242=PLANE('',#28620);
#2243=PLANE('',#28621);
#2244=PLANE('',#28622);
#2245=PLANE('',#28629);
#2246=PLANE('',#28630);
#2247=PLANE('',#28637);
#2248=PLANE('',#28638);
#2249=PLANE('',#28639);
#2250=PLANE('',#28640);
#3648=FACE_OUTER_BOUND('',#5393,.T.);
#3649=FACE_OUTER_BOUND('',#5394,.T.);
#3650=FACE_OUTER_BOUND('',#5395,.T.);
#3651=FACE_OUTER_BOUND('',#5396,.T.);
#3652=FACE_OUTER_BOUND('',#5397,.T.);
#3653=FACE_OUTER_BOUND('',#5398,.T.);
#3654=FACE_OUTER_BOUND('',#5400,.T.);
#3655=FACE_OUTER_BOUND('',#5401,.T.);
#3656=FACE_OUTER_BOUND('',#5403,.T.);
#3657=FACE_OUTER_BOUND('',#5405,.T.);
#3658=FACE_OUTER_BOUND('',#5406,.T.);
#3659=FACE_OUTER_BOUND('',#5407,.T.);
#3660=FACE_OUTER_BOUND('',#5408,.T.);
#3661=FACE_OUTER_BOUND('',#5409,.T.);
#3662=FACE_OUTER_BOUND('',#5410,.T.);
#3663=FACE_OUTER_BOUND('',#5411,.T.);
#3664=FACE_OUTER_BOUND('',#5412,.T.);
#3665=FACE_OUTER_BOUND('',#5413,.T.);
#3666=FACE_OUTER_BOUND('',#5414,.T.);
#3667=FACE_OUTER_BOUND('',#5415,.T.);
#3668=FACE_OUTER_BOUND('',#5416,.T.);
#3669=FACE_OUTER_BOUND('',#5417,.T.);
#3670=FACE_OUTER_BOUND('',#5418,.T.);
#3671=FACE_OUTER_BOUND('',#5419,.T.);
#3672=FACE_OUTER_BOUND('',#5421,.T.);
#3673=FACE_OUTER_BOUND('',#5423,.T.);
#3674=FACE_OUTER_BOUND('',#5424,.T.);
#3675=FACE_OUTER_BOUND('',#5425,.T.);
#3676=FACE_OUTER_BOUND('',#5426,.T.);
#3677=FACE_OUTER_BOUND('',#5427,.T.);
#3678=FACE_OUTER_BOUND('',#5428,.T.);
#5393=EDGE_LOOP('',(#23524,#23525,#23526,#23527,#23528));
#5394=EDGE_LOOP('',(#23529,#23530,#23531,#23532,#23533,#23534,#23535,#23536,
#23537));
#5395=EDGE_LOOP('',(#23538,#23539,#23540,#23541,#23542));
#5396=EDGE_LOOP('',(#23543,#23544,#23545,#23546));
#5397=EDGE_LOOP('',(#23547,#23548,#23549,#23550));
#5398=EDGE_LOOP('',(#23551));
#5399=EDGE_LOOP('',(#23552,#23553,#23554,#23555,#23556,#23557));
#5400=EDGE_LOOP('',(#23558));
#5401=EDGE_LOOP('',(#23559));
#5402=EDGE_LOOP('',(#23560));
#5403=EDGE_LOOP('',(#23561));
#5404=EDGE_LOOP('',(#23562));
#5405=EDGE_LOOP('',(#23563,#23564,#23565,#23566,#23567));
#5406=EDGE_LOOP('',(#23568,#23569,#23570,#23571,#23572));
#5407=EDGE_LOOP('',(#23573,#23574,#23575,#23576,#23577));
#5408=EDGE_LOOP('',(#23578,#23579,#23580,#23581,#23582));
#5409=EDGE_LOOP('',(#23583,#23584,#23585,#23586,#23587));
#5410=EDGE_LOOP('',(#23588,#23589,#23590,#23591,#23592));
#5411=EDGE_LOOP('',(#23593,#23594,#23595));
#5412=EDGE_LOOP('',(#23596,#23597,#23598,#23599));
#5413=EDGE_LOOP('',(#23600,#23601,#23602));
#5414=EDGE_LOOP('',(#23603,#23604,#23605));
#5415=EDGE_LOOP('',(#23606,#23607,#23608));
#5416=EDGE_LOOP('',(#23609,#23610,#23611));
#5417=EDGE_LOOP('',(#23612,#23613,#23614,#23615));
#5418=EDGE_LOOP('',(#23616,#23617,#23618,#23619));
#5419=EDGE_LOOP('',(#23620));
#5420=EDGE_LOOP('',(#23621));
#5421=EDGE_LOOP('',(#23622));
#5422=EDGE_LOOP('',(#23623));
#5423=EDGE_LOOP('',(#23624,#23625,#23626,#23627));
#5424=EDGE_LOOP('',(#23628,#23629,#23630,#23631));
#5425=EDGE_LOOP('',(#23632,#23633,#23634,#23635));
#5426=EDGE_LOOP('',(#23636,#23637,#23638,#23639));
#5427=EDGE_LOOP('',(#23640,#23641,#23642,#23643));
#5428=EDGE_LOOP('',(#23644,#23645,#23646,#23647));
#7383=LINE('',#66297,#9372);
#7384=LINE('',#66302,#9373);
#7385=LINE('',#66318,#9374);
#7386=LINE('',#66324,#9375);
#7387=LINE('',#66330,#9376);
#7388=LINE('',#66335,#9377);
#7389=LINE('',#66337,#9378);
#7390=LINE('',#66339,#9379);
#7391=LINE('',#66341,#9380);
#7392=LINE('',#66343,#9381);
#7393=LINE('',#66344,#9382);
#7394=LINE('',#66350,#9383);
#7395=LINE('',#66351,#9384);
#7396=LINE('',#66353,#9385);
#7397=LINE('',#66354,#9386);
#7398=LINE('',#66357,#9387);
#7399=LINE('',#66358,#9388);
#7400=LINE('',#66359,#9389);
#7401=LINE('',#66362,#9390);
#7402=LINE('',#66363,#9391);
#7403=LINE('',#66364,#9392);
#7404=LINE('',#66367,#9393);
#7405=LINE('',#66368,#9394);
#7406=LINE('',#66369,#9395);
#7407=LINE('',#66372,#9396);
#7408=LINE('',#66373,#9397);
#7409=LINE('',#66374,#9398);
#7410=LINE('',#66376,#9399);
#7411=LINE('',#66377,#9400);
#7412=LINE('',#66388,#9401);
#7413=LINE('',#66394,#9402);
#7414=LINE('',#66403,#9403);
#7415=LINE('',#66406,#9404);
#7416=LINE('',#66412,#9405);
#7417=LINE('',#66415,#9406);
#7418=LINE('',#66417,#9407);
#7419=LINE('',#66418,#9408);
#7420=LINE('',#66420,#9409);
#7421=LINE('',#66421,#9410);
#9372=VECTOR('',#35754,3.75);
#9373=VECTOR('',#35759,1664.2794823505);
#9374=VECTOR('',#35776,4.25);
#9375=VECTOR('',#35783,2.065);
#9376=VECTOR('',#35790,3.);
#9377=VECTOR('',#35795,1000.);
#9378=VECTOR('',#35796,1000.);
#9379=VECTOR('',#35797,1000.);
#9380=VECTOR('',#35798,1000.);
#9381=VECTOR('',#35799,1000.);
#9382=VECTOR('',#35800,1000.);
#9383=VECTOR('',#35809,1000.);
#9384=VECTOR('',#35810,1000.);
#9385=VECTOR('',#35811,1000.);
#9386=VECTOR('',#35812,1000.);
#9387=VECTOR('',#35815,1000.);
#9388=VECTOR('',#35816,1000.);
#9389=VECTOR('',#35817,1000.);
#9390=VECTOR('',#35820,1000.);
#9391=VECTOR('',#35821,1000.);
#9392=VECTOR('',#35822,1000.);
#9393=VECTOR('',#35825,1000.);
#9394=VECTOR('',#35826,1000.);
#9395=VECTOR('',#35827,1000.);
#9396=VECTOR('',#35830,1000.);
#9397=VECTOR('',#35831,1000.);
#9398=VECTOR('',#35832,1000.);
#9399=VECTOR('',#35835,1000.);
#9400=VECTOR('',#35836,1000.);
#9401=VECTOR('',#35853,5.);
#9402=VECTOR('',#35860,2.5);
#9403=VECTOR('',#35871,1000.);
#9404=VECTOR('',#35874,1000.);
#9405=VECTOR('',#35879,1000.);
#9406=VECTOR('',#35882,1000.);
#9407=VECTOR('',#35885,1000.);
#9408=VECTOR('',#35886,1000.);
#9409=VECTOR('',#35889,1000.);
#9410=VECTOR('',#35890,1000.);
#10588=CIRCLE('',#28588,4.25);
#10589=CIRCLE('',#28589,4.25);
#10590=CIRCLE('',#28590,3.75);
#10591=CIRCLE('',#28592,2.);
#10592=CIRCLE('',#28593,2.);
#10593=CIRCLE('',#28594,2.);
#10594=CIRCLE('',#28595,2.);
#10595=CIRCLE('',#28596,2.);
#10596=CIRCLE('',#28597,2.);
#10597=CIRCLE('',#28598,2.);
#10598=CIRCLE('',#28600,4.25);
#10599=CIRCLE('',#28602,2.065);
#10600=CIRCLE('',#28603,2.065);
#10601=CIRCLE('',#28605,3.);
#10602=CIRCLE('',#28606,3.);
#10603=CIRCLE('',#28624,5.);
#10604=CIRCLE('',#28625,5.);
#10605=CIRCLE('',#28627,2.5);
#10606=CIRCLE('',#28628,2.5);
#10607=CIRCLE('',#28632,4.25);
#10608=CIRCLE('',#28633,4.25);
#10609=CIRCLE('',#28635,2.5);
#10610=CIRCLE('',#28636,2.5);
#12899=VERTEX_POINT('',#66292);
#12900=VERTEX_POINT('',#66293);
#12901=VERTEX_POINT('',#66296);
#12902=VERTEX_POINT('',#66300);
#12903=VERTEX_POINT('',#66301);
#12904=VERTEX_POINT('',#66303);
#12905=VERTEX_POINT('',#66305);
#12906=VERTEX_POINT('',#66307);
#12907=VERTEX_POINT('',#66309);
#12908=VERTEX_POINT('',#66311);
#12909=VERTEX_POINT('',#66313);
#12910=VERTEX_POINT('',#66317);
#12911=VERTEX_POINT('',#66321);
#12912=VERTEX_POINT('',#66323);
#12913=VERTEX_POINT('',#66327);
#12914=VERTEX_POINT('',#66329);
#12915=VERTEX_POINT('',#66333);
#12916=VERTEX_POINT('',#66334);
#12917=VERTEX_POINT('',#66336);
#12918=VERTEX_POINT('',#66338);
#12919=VERTEX_POINT('',#66340);
#12920=VERTEX_POINT('',#66342);
#12921=VERTEX_POINT('',#66349);
#12922=VERTEX_POINT('',#66352);
#12923=VERTEX_POINT('',#66356);
#12924=VERTEX_POINT('',#66361);
#12925=VERTEX_POINT('',#66366);
#12926=VERTEX_POINT('',#66371);
#12927=VERTEX_POINT('',#66385);
#12928=VERTEX_POINT('',#66387);
#12929=VERTEX_POINT('',#66391);
#12930=VERTEX_POINT('',#66393);
#12931=VERTEX_POINT('',#66399);
#12932=VERTEX_POINT('',#66400);
#12933=VERTEX_POINT('',#66402);
#12934=VERTEX_POINT('',#66404);
#12935=VERTEX_POINT('',#66408);
#12936=VERTEX_POINT('',#66409);
#12937=VERTEX_POINT('',#66411);
#12938=VERTEX_POINT('',#66413);
#16455=EDGE_CURVE('',#12899,#12900,#10588,.T.);
#16456=EDGE_CURVE('',#12900,#12899,#10589,.T.);
#16457=EDGE_CURVE('',#12900,#12901,#7383,.T.);
#16458=EDGE_CURVE('',#12901,#12901,#10590,.T.);
#16459=EDGE_CURVE('',#12902,#12903,#7384,.T.);
#16460=EDGE_CURVE('',#12903,#12904,#10591,.T.);
#16461=EDGE_CURVE('',#12904,#12905,#10592,.T.);
#16462=EDGE_CURVE('',#12905,#12906,#10593,.T.);
#16463=EDGE_CURVE('',#12906,#12907,#10594,.T.);
#16464=EDGE_CURVE('',#12907,#12908,#10595,.T.);
#16465=EDGE_CURVE('',#12908,#12909,#10596,.T.);
#16466=EDGE_CURVE('',#12909,#12903,#10597,.T.);
#16467=EDGE_CURVE('',#12899,#12910,#7385,.T.);
#16468=EDGE_CURVE('',#12910,#12910,#10598,.T.);
#16469=EDGE_CURVE('',#12911,#12911,#10599,.T.);
#16470=EDGE_CURVE('',#12911,#12912,#7386,.T.);
#16471=EDGE_CURVE('',#12912,#12912,#10600,.T.);
#16472=EDGE_CURVE('',#12913,#12913,#10601,.T.);
#16473=EDGE_CURVE('',#12913,#12914,#7387,.T.);
#16474=EDGE_CURVE('',#12914,#12914,#10602,.T.);
#16475=EDGE_CURVE('',#12915,#12916,#7388,.T.);
#16476=EDGE_CURVE('',#12917,#12915,#7389,.T.);
#16477=EDGE_CURVE('',#12918,#12917,#7390,.T.);
#16478=EDGE_CURVE('',#12919,#12918,#7391,.T.);
#16479=EDGE_CURVE('',#12920,#12919,#7392,.T.);
#16480=EDGE_CURVE('',#12916,#12920,#7393,.T.);
#16481=EDGE_CURVE('',#12921,#12908,#7394,.T.);
#16482=EDGE_CURVE('',#12921,#12917,#7395,.T.);
#16483=EDGE_CURVE('',#12922,#12915,#7396,.T.);
#16484=EDGE_CURVE('',#12908,#12922,#7397,.T.);
#16485=EDGE_CURVE('',#12923,#12907,#7398,.T.);
#16486=EDGE_CURVE('',#12923,#12918,#7399,.T.);
#16487=EDGE_CURVE('',#12907,#12921,#7400,.T.);
#16488=EDGE_CURVE('',#12924,#12906,#7401,.T.);
#16489=EDGE_CURVE('',#12924,#12919,#7402,.T.);
#16490=EDGE_CURVE('',#12906,#12923,#7403,.T.);
#16491=EDGE_CURVE('',#12925,#12905,#7404,.T.);
#16492=EDGE_CURVE('',#12925,#12920,#7405,.T.);
#16493=EDGE_CURVE('',#12905,#12924,#7406,.T.);
#16494=EDGE_CURVE('',#12926,#12904,#7407,.T.);
#16495=EDGE_CURVE('',#12926,#12916,#7408,.T.);
#16496=EDGE_CURVE('',#12904,#12925,#7409,.T.);
#16497=EDGE_CURVE('',#12922,#12909,#7410,.T.);
#16498=EDGE_CURVE('',#12909,#12926,#7411,.T.);
#16499=EDGE_CURVE('',#12927,#12927,#10603,.T.);
#16500=EDGE_CURVE('',#12927,#12928,#7412,.T.);
#16501=EDGE_CURVE('',#12928,#12928,#10604,.T.);
#16502=EDGE_CURVE('',#12929,#12929,#10605,.T.);
#16503=EDGE_CURVE('',#12929,#12930,#7413,.T.);
#16504=EDGE_CURVE('',#12930,#12930,#10606,.T.);
#16505=EDGE_CURVE('',#12931,#12932,#10607,.T.);
#16506=EDGE_CURVE('',#12933,#12932,#7414,.T.);
#16507=EDGE_CURVE('',#12934,#12933,#10608,.T.);
#16508=EDGE_CURVE('',#12934,#12931,#7415,.T.);
#16509=EDGE_CURVE('',#12935,#12936,#10609,.T.);
#16510=EDGE_CURVE('',#12937,#12935,#7416,.T.);
#16511=EDGE_CURVE('',#12937,#12938,#10610,.T.);
#16512=EDGE_CURVE('',#12938,#12936,#7417,.T.);
#16513=EDGE_CURVE('',#12933,#12938,#7418,.T.);
#16514=EDGE_CURVE('',#12937,#12934,#7419,.T.);
#16515=EDGE_CURVE('',#12932,#12936,#7420,.T.);
#16516=EDGE_CURVE('',#12935,#12931,#7421,.T.);
#23524=ORIENTED_EDGE('',*,*,#16455,.F.);
#23525=ORIENTED_EDGE('',*,*,#16456,.F.);
#23526=ORIENTED_EDGE('',*,*,#16457,.T.);
#23527=ORIENTED_EDGE('',*,*,#16458,.F.);
#23528=ORIENTED_EDGE('',*,*,#16457,.F.);
#23529=ORIENTED_EDGE('',*,*,#16459,.T.);
#23530=ORIENTED_EDGE('',*,*,#16460,.T.);
#23531=ORIENTED_EDGE('',*,*,#16461,.T.);
#23532=ORIENTED_EDGE('',*,*,#16462,.T.);
#23533=ORIENTED_EDGE('',*,*,#16463,.T.);
#23534=ORIENTED_EDGE('',*,*,#16464,.T.);
#23535=ORIENTED_EDGE('',*,*,#16465,.T.);
#23536=ORIENTED_EDGE('',*,*,#16466,.T.);
#23537=ORIENTED_EDGE('',*,*,#16459,.F.);
#23538=ORIENTED_EDGE('',*,*,#16455,.T.);
#23539=ORIENTED_EDGE('',*,*,#16456,.T.);
#23540=ORIENTED_EDGE('',*,*,#16467,.T.);
#23541=ORIENTED_EDGE('',*,*,#16468,.T.);
#23542=ORIENTED_EDGE('',*,*,#16467,.F.);
#23543=ORIENTED_EDGE('',*,*,#16469,.F.);
#23544=ORIENTED_EDGE('',*,*,#16470,.T.);
#23545=ORIENTED_EDGE('',*,*,#16471,.T.);
#23546=ORIENTED_EDGE('',*,*,#16470,.F.);
#23547=ORIENTED_EDGE('',*,*,#16472,.F.);
#23548=ORIENTED_EDGE('',*,*,#16473,.T.);
#23549=ORIENTED_EDGE('',*,*,#16474,.T.);
#23550=ORIENTED_EDGE('',*,*,#16473,.F.);
#23551=ORIENTED_EDGE('',*,*,#16458,.T.);
#23552=ORIENTED_EDGE('',*,*,#16475,.F.);
#23553=ORIENTED_EDGE('',*,*,#16476,.F.);
#23554=ORIENTED_EDGE('',*,*,#16477,.F.);
#23555=ORIENTED_EDGE('',*,*,#16478,.F.);
#23556=ORIENTED_EDGE('',*,*,#16479,.F.);
#23557=ORIENTED_EDGE('',*,*,#16480,.F.);
#23558=ORIENTED_EDGE('',*,*,#16474,.F.);
#23559=ORIENTED_EDGE('',*,*,#16472,.T.);
#23560=ORIENTED_EDGE('',*,*,#16471,.F.);
#23561=ORIENTED_EDGE('',*,*,#16468,.F.);
#23562=ORIENTED_EDGE('',*,*,#16469,.T.);
#23563=ORIENTED_EDGE('',*,*,#16481,.F.);
#23564=ORIENTED_EDGE('',*,*,#16482,.T.);
#23565=ORIENTED_EDGE('',*,*,#16476,.T.);
#23566=ORIENTED_EDGE('',*,*,#16483,.F.);
#23567=ORIENTED_EDGE('',*,*,#16484,.F.);
#23568=ORIENTED_EDGE('',*,*,#16485,.F.);
#23569=ORIENTED_EDGE('',*,*,#16486,.T.);
#23570=ORIENTED_EDGE('',*,*,#16477,.T.);
#23571=ORIENTED_EDGE('',*,*,#16482,.F.);
#23572=ORIENTED_EDGE('',*,*,#16487,.F.);
#23573=ORIENTED_EDGE('',*,*,#16488,.F.);
#23574=ORIENTED_EDGE('',*,*,#16489,.T.);
#23575=ORIENTED_EDGE('',*,*,#16478,.T.);
#23576=ORIENTED_EDGE('',*,*,#16486,.F.);
#23577=ORIENTED_EDGE('',*,*,#16490,.F.);
#23578=ORIENTED_EDGE('',*,*,#16491,.F.);
#23579=ORIENTED_EDGE('',*,*,#16492,.T.);
#23580=ORIENTED_EDGE('',*,*,#16479,.T.);
#23581=ORIENTED_EDGE('',*,*,#16489,.F.);
#23582=ORIENTED_EDGE('',*,*,#16493,.F.);
#23583=ORIENTED_EDGE('',*,*,#16494,.F.);
#23584=ORIENTED_EDGE('',*,*,#16495,.T.);
#23585=ORIENTED_EDGE('',*,*,#16480,.T.);
#23586=ORIENTED_EDGE('',*,*,#16492,.F.);
#23587=ORIENTED_EDGE('',*,*,#16496,.F.);
#23588=ORIENTED_EDGE('',*,*,#16497,.F.);
#23589=ORIENTED_EDGE('',*,*,#16483,.T.);
#23590=ORIENTED_EDGE('',*,*,#16475,.T.);
#23591=ORIENTED_EDGE('',*,*,#16495,.F.);
#23592=ORIENTED_EDGE('',*,*,#16498,.F.);
#23593=ORIENTED_EDGE('',*,*,#16484,.T.);
#23594=ORIENTED_EDGE('',*,*,#16497,.T.);
#23595=ORIENTED_EDGE('',*,*,#16465,.F.);
#23596=ORIENTED_EDGE('',*,*,#16498,.T.);
#23597=ORIENTED_EDGE('',*,*,#16494,.T.);
#23598=ORIENTED_EDGE('',*,*,#16460,.F.);
#23599=ORIENTED_EDGE('',*,*,#16466,.F.);
#23600=ORIENTED_EDGE('',*,*,#16496,.T.);
#23601=ORIENTED_EDGE('',*,*,#16491,.T.);
#23602=ORIENTED_EDGE('',*,*,#16461,.F.);
#23603=ORIENTED_EDGE('',*,*,#16493,.T.);
#23604=ORIENTED_EDGE('',*,*,#16488,.T.);
#23605=ORIENTED_EDGE('',*,*,#16462,.F.);
#23606=ORIENTED_EDGE('',*,*,#16490,.T.);
#23607=ORIENTED_EDGE('',*,*,#16485,.T.);
#23608=ORIENTED_EDGE('',*,*,#16463,.F.);
#23609=ORIENTED_EDGE('',*,*,#16487,.T.);
#23610=ORIENTED_EDGE('',*,*,#16481,.T.);
#23611=ORIENTED_EDGE('',*,*,#16464,.F.);
#23612=ORIENTED_EDGE('',*,*,#16499,.F.);
#23613=ORIENTED_EDGE('',*,*,#16500,.T.);
#23614=ORIENTED_EDGE('',*,*,#16501,.T.);
#23615=ORIENTED_EDGE('',*,*,#16500,.F.);
#23616=ORIENTED_EDGE('',*,*,#16502,.F.);
#23617=ORIENTED_EDGE('',*,*,#16503,.T.);
#23618=ORIENTED_EDGE('',*,*,#16504,.T.);
#23619=ORIENTED_EDGE('',*,*,#16503,.F.);
#23620=ORIENTED_EDGE('',*,*,#16499,.T.);
#23621=ORIENTED_EDGE('',*,*,#16504,.F.);
#23622=ORIENTED_EDGE('',*,*,#16501,.F.);
#23623=ORIENTED_EDGE('',*,*,#16502,.T.);
#23624=ORIENTED_EDGE('',*,*,#16505,.T.);
#23625=ORIENTED_EDGE('',*,*,#16506,.F.);
#23626=ORIENTED_EDGE('',*,*,#16507,.F.);
#23627=ORIENTED_EDGE('',*,*,#16508,.T.);
#23628=ORIENTED_EDGE('',*,*,#16509,.F.);
#23629=ORIENTED_EDGE('',*,*,#16510,.F.);
#23630=ORIENTED_EDGE('',*,*,#16511,.T.);
#23631=ORIENTED_EDGE('',*,*,#16512,.T.);
#23632=ORIENTED_EDGE('',*,*,#16507,.T.);
#23633=ORIENTED_EDGE('',*,*,#16513,.T.);
#23634=ORIENTED_EDGE('',*,*,#16511,.F.);
#23635=ORIENTED_EDGE('',*,*,#16514,.T.);
#23636=ORIENTED_EDGE('',*,*,#16509,.T.);
#23637=ORIENTED_EDGE('',*,*,#16515,.F.);
#23638=ORIENTED_EDGE('',*,*,#16505,.F.);
#23639=ORIENTED_EDGE('',*,*,#16516,.F.);
#23640=ORIENTED_EDGE('',*,*,#16516,.T.);
#23641=ORIENTED_EDGE('',*,*,#16508,.F.);
#23642=ORIENTED_EDGE('',*,*,#16514,.F.);
#23643=ORIENTED_EDGE('',*,*,#16510,.T.);
#23644=ORIENTED_EDGE('',*,*,#16515,.T.);
#23645=ORIENTED_EDGE('',*,*,#16512,.F.);
#23646=ORIENTED_EDGE('',*,*,#16513,.F.);
#23647=ORIENTED_EDGE('',*,*,#16506,.T.);
#24203=CYLINDRICAL_SURFACE('',#28599,4.25);
#24204=CYLINDRICAL_SURFACE('',#28601,2.065);
#24205=CYLINDRICAL_SURFACE('',#28604,3.);
#24206=CYLINDRICAL_SURFACE('',#28623,5.);
#24207=CYLINDRICAL_SURFACE('',#28626,2.5);
#24208=CYLINDRICAL_SURFACE('',#28631,4.25);
#24209=CYLINDRICAL_SURFACE('',#28634,2.5);
#25601=ADVANCED_FACE('',(#3648),#578,.T.);
#25602=ADVANCED_FACE('',(#3649),#579,.F.);
#25603=ADVANCED_FACE('',(#3650),#24203,.T.);
#25604=ADVANCED_FACE('',(#3651),#24204,.T.);
#25605=ADVANCED_FACE('',(#3652),#24205,.T.);
#25606=ADVANCED_FACE('',(#3653,#1471),#2229,.F.);
#25607=ADVANCED_FACE('',(#3654),#2230,.F.);
#25608=ADVANCED_FACE('',(#3655,#1472),#2231,.F.);
#25609=ADVANCED_FACE('',(#3656,#1473),#2232,.F.);
#25610=ADVANCED_FACE('',(#3657),#2233,.F.);
#25611=ADVANCED_FACE('',(#3658),#2234,.F.);
#25612=ADVANCED_FACE('',(#3659),#2235,.F.);
#25613=ADVANCED_FACE('',(#3660),#2236,.F.);
#25614=ADVANCED_FACE('',(#3661),#2237,.F.);
#25615=ADVANCED_FACE('',(#3662),#2238,.F.);
#25616=ADVANCED_FACE('',(#3663),#2239,.T.);
#25617=ADVANCED_FACE('',(#3664),#2240,.T.);
#25618=ADVANCED_FACE('',(#3665),#2241,.T.);
#25619=ADVANCED_FACE('',(#3666),#2242,.T.);
#25620=ADVANCED_FACE('',(#3667),#2243,.T.);
#25621=ADVANCED_FACE('',(#3668),#2244,.T.);
#25622=ADVANCED_FACE('',(#3669),#24206,.T.);
#25623=ADVANCED_FACE('',(#3670),#24207,.F.);
#25624=ADVANCED_FACE('',(#3671,#1474),#2245,.F.);
#25625=ADVANCED_FACE('',(#3672,#1475),#2246,.F.);
#25626=ADVANCED_FACE('',(#3673),#24208,.T.);
#25627=ADVANCED_FACE('',(#3674),#24209,.F.);
#25628=ADVANCED_FACE('',(#3675),#2247,.F.);
#25629=ADVANCED_FACE('',(#3676),#2248,.F.);
#25630=ADVANCED_FACE('',(#3677),#2249,.F.);
#25631=ADVANCED_FACE('',(#3678),#2250,.F.);
#25694=CLOSED_SHELL('',(#25601,#25602,#25603,#25604,#25605,#25606,#25607,
#25608,#25609,#25610,#25611,#25612,#25613,#25614,#25615,#25616,#25617,#25618,
#25619,#25620,#25621));
#25695=CLOSED_SHELL('',(#25622,#25623,#25624,#25625));
#25696=CLOSED_SHELL('',(#25626,#25627,#25628,#25629,#25630,#25631));
#28586=AXIS2_PLACEMENT_3D('',#66290,#35746,#35747);
#28587=AXIS2_PLACEMENT_3D('',#66291,#35748,#35749);
#28588=AXIS2_PLACEMENT_3D('',#66294,#35750,#35751);
#28589=AXIS2_PLACEMENT_3D('',#66295,#35752,#35753);
#28590=AXIS2_PLACEMENT_3D('',#66298,#35755,#35756);
#28591=AXIS2_PLACEMENT_3D('',#66299,#35757,#35758);
#28592=AXIS2_PLACEMENT_3D('',#66304,#35760,#35761);
#28593=AXIS2_PLACEMENT_3D('',#66306,#35762,#35763);
#28594=AXIS2_PLACEMENT_3D('',#66308,#35764,#35765);
#28595=AXIS2_PLACEMENT_3D('',#66310,#35766,#35767);
#28596=AXIS2_PLACEMENT_3D('',#66312,#35768,#35769);
#28597=AXIS2_PLACEMENT_3D('',#66314,#35770,#35771);
#28598=AXIS2_PLACEMENT_3D('',#66315,#35772,#35773);
#28599=AXIS2_PLACEMENT_3D('',#66316,#35774,#35775);
#28600=AXIS2_PLACEMENT_3D('',#66319,#35777,#35778);
#28601=AXIS2_PLACEMENT_3D('',#66320,#35779,#35780);
#28602=AXIS2_PLACEMENT_3D('',#66322,#35781,#35782);
#28603=AXIS2_PLACEMENT_3D('',#66325,#35784,#35785);
#28604=AXIS2_PLACEMENT_3D('',#66326,#35786,#35787);
#28605=AXIS2_PLACEMENT_3D('',#66328,#35788,#35789);
#28606=AXIS2_PLACEMENT_3D('',#66331,#35791,#35792);
#28607=AXIS2_PLACEMENT_3D('',#66332,#35793,#35794);
#28608=AXIS2_PLACEMENT_3D('',#66345,#35801,#35802);
#28609=AXIS2_PLACEMENT_3D('',#66346,#35803,#35804);
#28610=AXIS2_PLACEMENT_3D('',#66347,#35805,#35806);
#28611=AXIS2_PLACEMENT_3D('',#66348,#35807,#35808);
#28612=AXIS2_PLACEMENT_3D('',#66355,#35813,#35814);
#28613=AXIS2_PLACEMENT_3D('',#66360,#35818,#35819);
#28614=AXIS2_PLACEMENT_3D('',#66365,#35823,#35824);
#28615=AXIS2_PLACEMENT_3D('',#66370,#35828,#35829);
#28616=AXIS2_PLACEMENT_3D('',#66375,#35833,#35834);
#28617=AXIS2_PLACEMENT_3D('',#66378,#35837,#35838);
#28618=AXIS2_PLACEMENT_3D('',#66379,#35839,#35840);
#28619=AXIS2_PLACEMENT_3D('',#66380,#35841,#35842);
#28620=AXIS2_PLACEMENT_3D('',#66381,#35843,#35844);
#28621=AXIS2_PLACEMENT_3D('',#66382,#35845,#35846);
#28622=AXIS2_PLACEMENT_3D('',#66383,#35847,#35848);
#28623=AXIS2_PLACEMENT_3D('',#66384,#35849,#35850);
#28624=AXIS2_PLACEMENT_3D('',#66386,#35851,#35852);
#28625=AXIS2_PLACEMENT_3D('',#66389,#35854,#35855);
#28626=AXIS2_PLACEMENT_3D('',#66390,#35856,#35857);
#28627=AXIS2_PLACEMENT_3D('',#66392,#35858,#35859);
#28628=AXIS2_PLACEMENT_3D('',#66395,#35861,#35862);
#28629=AXIS2_PLACEMENT_3D('',#66396,#35863,#35864);
#28630=AXIS2_PLACEMENT_3D('',#66397,#35865,#35866);
#28631=AXIS2_PLACEMENT_3D('',#66398,#35867,#35868);
#28632=AXIS2_PLACEMENT_3D('',#66401,#35869,#35870);
#28633=AXIS2_PLACEMENT_3D('',#66405,#35872,#35873);
#28634=AXIS2_PLACEMENT_3D('',#66407,#35875,#35876);
#28635=AXIS2_PLACEMENT_3D('',#66410,#35877,#35878);
#28636=AXIS2_PLACEMENT_3D('',#66414,#35880,#35881);
#28637=AXIS2_PLACEMENT_3D('',#66416,#35883,#35884);
#28638=AXIS2_PLACEMENT_3D('',#66419,#35887,#35888);
#28639=AXIS2_PLACEMENT_3D('',#66422,#35891,#35892);
#28640=AXIS2_PLACEMENT_3D('',#66423,#35893,#35894);
#35746=DIRECTION('axis',(0.,0.,1.));
#35747=DIRECTION('refdir',(1.,0.,0.));
#35748=DIRECTION('center_axis',(1.,0.,0.));
#35749=DIRECTION('ref_axis',(0.,0.,-1.));
#35750=DIRECTION('center_axis',(1.,0.,0.));
#35751=DIRECTION('ref_axis',(0.,0.,-1.));
#35752=DIRECTION('center_axis',(1.,0.,0.));
#35753=DIRECTION('ref_axis',(0.,0.,-1.));
#35754=DIRECTION('',(-0.70710678118655,8.65956056235489E-17,-0.707106781186544));
#35755=DIRECTION('center_axis',(-1.,0.,0.));
#35756=DIRECTION('ref_axis',(0.,0.,-1.));
#35757=DIRECTION('center_axis',(-1.,5.24877093477881E-17,0.));
#35758=DIRECTION('ref_axis',(-5.24877093477881E-17,-1.,0.));
#35759=DIRECTION('',(-0.515038074910058,0.85716730070211,-1.04972719113862E-16));
#35760=DIRECTION('center_axis',(-1.,5.24877093477881E-17,0.));
#35761=DIRECTION('ref_axis',(-5.24877093477881E-17,-1.,0.));
#35762=DIRECTION('center_axis',(-1.,5.24877093477881E-17,0.));
#35763=DIRECTION('ref_axis',(-5.24877093477881E-17,-1.,0.));
#35764=DIRECTION('center_axis',(-1.,5.24877093477881E-17,0.));
#35765=DIRECTION('ref_axis',(-5.24877093477881E-17,-1.,0.));
#35766=DIRECTION('center_axis',(-1.,5.24877093477881E-17,0.));
#35767=DIRECTION('ref_axis',(-5.24877093477881E-17,-1.,0.));
#35768=DIRECTION('center_axis',(-1.,5.24877093477881E-17,0.));
#35769=DIRECTION('ref_axis',(-5.24877093477881E-17,-1.,0.));
#35770=DIRECTION('center_axis',(-1.,5.24877093477881E-17,0.));
#35771=DIRECTION('ref_axis',(-5.24877093477881E-17,-1.,0.));
#35772=DIRECTION('center_axis',(-1.,5.24877093477881E-17,0.));
#35773=DIRECTION('ref_axis',(-5.24877093477881E-17,-1.,0.));
#35774=DIRECTION('center_axis',(-1.,0.,0.));
#35775=DIRECTION('ref_axis',(0.,0.,1.));
#35776=DIRECTION('',(1.,0.,0.));
#35777=DIRECTION('center_axis',(-1.,0.,0.));
#35778=DIRECTION('ref_axis',(0.,0.,1.));
#35779=DIRECTION('center_axis',(-1.,0.,0.));
#35780=DIRECTION('ref_axis',(0.,0.,1.));
#35781=DIRECTION('center_axis',(-1.,0.,0.));
#35782=DIRECTION('ref_axis',(0.,0.,1.));
#35783=DIRECTION('',(1.,0.,0.));
#35784=DIRECTION('center_axis',(-1.,0.,0.));
#35785=DIRECTION('ref_axis',(0.,0.,1.));
#35786=DIRECTION('center_axis',(-1.,0.,0.));
#35787=DIRECTION('ref_axis',(0.,0.,1.));
#35788=DIRECTION('center_axis',(-1.,0.,0.));
#35789=DIRECTION('ref_axis',(0.,0.,1.));
#35790=DIRECTION('',(1.,0.,0.));
#35791=DIRECTION('center_axis',(-1.,0.,0.));
#35792=DIRECTION('ref_axis',(0.,0.,1.));
#35793=DIRECTION('center_axis',(1.,0.,0.));
#35794=DIRECTION('ref_axis',(0.,0.,-1.));
#35795=DIRECTION('',(0.,0.5,-0.866025403784439));
#35796=DIRECTION('',(0.,1.,-1.87789324842145E-16));
#35797=DIRECTION('',(0.,0.5,0.866025403784439));
#35798=DIRECTION('',(0.,-0.5,0.866025403784439));
#35799=DIRECTION('',(0.,-1.,0.));
#35800=DIRECTION('',(0.,-0.5,-0.866025403784439));
#35801=DIRECTION('center_axis',(-1.,0.,0.));
#35802=DIRECTION('ref_axis',(0.,0.,1.));
#35803=DIRECTION('center_axis',(1.,0.,0.));
#35804=DIRECTION('ref_axis',(0.,0.,-1.));
#35805=DIRECTION('center_axis',(-1.,0.,0.));
#35806=DIRECTION('ref_axis',(0.,0.,1.));
#35807=DIRECTION('center_axis',(0.,1.87789324842145E-16,1.));
#35808=DIRECTION('ref_axis',(0.,-1.,1.87789324842145E-16));
#35809=DIRECTION('',(0.,1.,-1.87789324842145E-16));
#35810=DIRECTION('',(-1.,0.,0.));
#35811=DIRECTION('',(-1.,0.,0.));
#35812=DIRECTION('',(0.,1.,-1.87789324842145E-16));
#35813=DIRECTION('center_axis',(0.,-0.866025403784439,0.5));
#35814=DIRECTION('ref_axis',(0.,-0.5,-0.866025403784439));
#35815=DIRECTION('',(0.,0.5,0.866025403784439));
#35816=DIRECTION('',(-1.,0.,0.));
#35817=DIRECTION('',(0.,0.5,0.866025403784439));
#35818=DIRECTION('center_axis',(0.,-0.866025403784439,-0.5));
#35819=DIRECTION('ref_axis',(0.,0.5,-0.866025403784439));
#35820=DIRECTION('',(0.,-0.5,0.866025403784439));
#35821=DIRECTION('',(-1.,0.,0.));
#35822=DIRECTION('',(0.,-0.5,0.866025403784439));
#35823=DIRECTION('center_axis',(0.,0.,-1.));
#35824=DIRECTION('ref_axis',(-1.,0.,0.));
#35825=DIRECTION('',(0.,-1.,0.));
#35826=DIRECTION('',(-1.,0.,0.));
#35827=DIRECTION('',(0.,-1.,0.));
#35828=DIRECTION('center_axis',(0.,0.866025403784439,-0.5));
#35829=DIRECTION('ref_axis',(0.,0.5,0.866025403784439));
#35830=DIRECTION('',(0.,-0.5,-0.866025403784439));
#35831=DIRECTION('',(-1.,0.,0.));
#35832=DIRECTION('',(0.,-0.5,-0.866025403784439));
#35833=DIRECTION('center_axis',(0.,0.866025403784439,0.5));
#35834=DIRECTION('ref_axis',(0.,-0.5,0.866025403784439));
#35835=DIRECTION('',(0.,0.5,-0.866025403784439));
#35836=DIRECTION('',(0.,0.5,-0.866025403784439));
#35837=DIRECTION('center_axis',(-1.,0.,0.));
#35838=DIRECTION('ref_axis',(0.,0.,1.));
#35839=DIRECTION('center_axis',(-1.,0.,0.));
#35840=DIRECTION('ref_axis',(0.,0.,1.));
#35841=DIRECTION('center_axis',(-1.,0.,0.));
#35842=DIRECTION('ref_axis',(0.,0.,1.));
#35843=DIRECTION('center_axis',(-1.,0.,0.));
#35844=DIRECTION('ref_axis',(0.,0.,1.));
#35845=DIRECTION('center_axis',(-1.,0.,0.));
#35846=DIRECTION('ref_axis',(0.,0.,1.));
#35847=DIRECTION('center_axis',(-1.,0.,0.));
#35848=DIRECTION('ref_axis',(0.,0.,1.));
#35849=DIRECTION('center_axis',(-1.,-3.84779799073557E-18,0.));
#35850=DIRECTION('ref_axis',(3.84779799073557E-18,-1.,0.));
#35851=DIRECTION('center_axis',(-1.,-3.84779799073557E-18,0.));
#35852=DIRECTION('ref_axis',(3.84779799073557E-18,-1.,0.));
#35853=DIRECTION('',(1.,3.84779799073557E-18,0.));
#35854=DIRECTION('center_axis',(-1.,-3.84779799073557E-18,0.));
#35855=DIRECTION('ref_axis',(3.84779799073557E-18,-1.,0.));
#35856=DIRECTION('center_axis',(-1.,-3.84779799073557E-18,0.));
#35857=DIRECTION('ref_axis',(3.84779799073557E-18,-1.,0.));
#35858=DIRECTION('center_axis',(-1.,-3.84779799073557E-18,0.));
#35859=DIRECTION('ref_axis',(3.84779799073557E-18,-1.,0.));
#35860=DIRECTION('',(-1.,-3.84779799073557E-18,0.));
#35861=DIRECTION('center_axis',(-1.,-3.84779799073557E-18,0.));
#35862=DIRECTION('ref_axis',(3.84779799073557E-18,-1.,0.));
#35863=DIRECTION('center_axis',(1.,3.84779799073557E-18,0.));
#35864=DIRECTION('ref_axis',(-3.84779799073557E-18,1.,0.));
#35865=DIRECTION('center_axis',(-1.,-3.84779799073557E-18,0.));
#35866=DIRECTION('ref_axis',(3.84779799073557E-18,-1.,0.));
#35867=DIRECTION('center_axis',(-1.,-1.22125762314651E-17,0.));
#35868=DIRECTION('ref_axis',(-3.62527989531715E-33,1.83697019872103E-16,
-1.));
#35869=DIRECTION('center_axis',(-1.,-1.22125762314651E-17,0.));
#35870=DIRECTION('ref_axis',(1.22125762314651E-17,-1.,0.));
#35871=DIRECTION('',(1.,0.,0.));
#35872=DIRECTION('center_axis',(-1.,-1.22125762314651E-17,0.));
#35873=DIRECTION('ref_axis',(1.22125762314651E-17,-1.,0.));
#35874=DIRECTION('',(1.,0.,0.));
#35875=DIRECTION('center_axis',(-1.,-1.22125762314651E-17,0.));
#35876=DIRECTION('ref_axis',(-3.08148791101958E-33,1.83697019872103E-16,
-1.));
#35877=DIRECTION('center_axis',(-1.,-1.22125762314651E-17,0.));
#35878=DIRECTION('ref_axis',(1.22125762314651E-17,-1.,0.));
#35879=DIRECTION('',(1.,0.,0.));
#35880=DIRECTION('center_axis',(-1.,-1.22125762314651E-17,0.));
#35881=DIRECTION('ref_axis',(1.22125762314651E-17,-1.,0.));
#35882=DIRECTION('',(1.,0.,0.));
#35883=DIRECTION('center_axis',(1.,1.22125762314651E-17,0.));
#35884=DIRECTION('ref_axis',(-1.22125762314651E-17,1.,0.));
#35885=DIRECTION('',(0.,0.,-1.));
#35886=DIRECTION('',(0.,0.,1.));
#35887=DIRECTION('center_axis',(-1.,-1.22125762314651E-17,0.));
#35888=DIRECTION('ref_axis',(1.22125762314651E-17,-1.,0.));
#35889=DIRECTION('',(0.,0.,-1.));
#35890=DIRECTION('',(0.,0.,1.));
#35891=DIRECTION('center_axis',(0.,1.,0.));
#35892=DIRECTION('ref_axis',(0.,0.,1.));
#35893=DIRECTION('center_axis',(0.,-1.,0.));
#35894=DIRECTION('ref_axis',(0.,0.,-1.));
#66290=CARTESIAN_POINT('',(0.,0.,0.));
#66291=CARTESIAN_POINT('Origin',(-7.3,0.,0.));
#66292=CARTESIAN_POINT('',(-6.79999999999999,5.20474889637625E-16,-4.25));
#66293=CARTESIAN_POINT('',(-6.79999999999999,-5.20474889637625E-16,4.25));
#66294=CARTESIAN_POINT('Origin',(-6.79999999999999,0.,0.));
#66295=CARTESIAN_POINT('Origin',(-6.79999999999999,0.,0.));
#66296=CARTESIAN_POINT('',(-7.3,-4.59242549680257E-16,3.75));
#66297=CARTESIAN_POINT('',(-7.3,-4.59242549680257E-16,3.75));
#66298=CARTESIAN_POINT('Origin',(-7.3,0.,0.));
#66299=CARTESIAN_POINT('Origin',(-1003.59827876194,5.22934144793585E-14,
0.));
#66300=CARTESIAN_POINT('',(-3.59827876194487,-1.94294868429572E-16,0.));
#66301=CARTESIAN_POINT('',(-4.80000000000004,2.00000000000045,-2.44929359829514E-16));
#66302=CARTESIAN_POINT('',(-1003.59827876194,1664.2794823505,-2.03815454094715E-13));
#66303=CARTESIAN_POINT('',(-4.8,1.73205080756888,-1.));
#66304=CARTESIAN_POINT('Origin',(-4.8,-1.3121927336947E-16,0.));
#66305=CARTESIAN_POINT('',(-4.8,-1.3121927336947E-16,-2.));
#66306=CARTESIAN_POINT('Origin',(-4.8,-1.3121927336947E-16,0.));
#66307=CARTESIAN_POINT('',(-4.8,-1.73205080756888,-1.));
#66308=CARTESIAN_POINT('Origin',(-4.8,-1.3121927336947E-16,0.));
#66309=CARTESIAN_POINT('',(-4.8,-1.73205080756888,1.));
#66310=CARTESIAN_POINT('Origin',(-4.8,-1.3121927336947E-16,0.));
#66311=CARTESIAN_POINT('',(-4.8,2.4435937631482E-16,2.));
#66312=CARTESIAN_POINT('Origin',(-4.8,-1.3121927336947E-16,0.));
#66313=CARTESIAN_POINT('',(-4.8,1.73205080756888,0.999999999999999));
#66314=CARTESIAN_POINT('Origin',(-4.8,-1.3121927336947E-16,0.));
#66315=CARTESIAN_POINT('Origin',(-4.8,-1.3121927336947E-16,0.));
#66316=CARTESIAN_POINT('Origin',(-7.3,0.,0.));
#66317=CARTESIAN_POINT('',(-2.3,-5.20474889637625E-16,-4.25));
#66318=CARTESIAN_POINT('',(-7.3,-5.20474889637625E-16,-4.25));
#66319=CARTESIAN_POINT('Origin',(-2.3,0.,0.));
#66320=CARTESIAN_POINT('Origin',(-7.3,0.,0.));
#66321=CARTESIAN_POINT('',(-2.3,-2.52889564023928E-16,-2.065));
#66322=CARTESIAN_POINT('Origin',(-2.3,0.,0.));
#66323=CARTESIAN_POINT('',(2.85,-2.52889564023928E-16,-2.065));
#66324=CARTESIAN_POINT('',(-7.3,-2.52889564023928E-16,-2.065));
#66325=CARTESIAN_POINT('Origin',(2.85,0.,0.));
#66326=CARTESIAN_POINT('Origin',(-7.3,0.,0.));
#66327=CARTESIAN_POINT('',(2.85,-3.67394039744206E-16,-3.));
#66328=CARTESIAN_POINT('Origin',(2.85,0.,0.));
#66329=CARTESIAN_POINT('',(22.7,-3.67394039744206E-16,-3.));
#66330=CARTESIAN_POINT('',(-7.3,-3.67394039744206E-16,-3.));
#66331=CARTESIAN_POINT('Origin',(22.7,0.,0.));
#66332=CARTESIAN_POINT('Origin',(-7.3,0.,0.));
#66333=CARTESIAN_POINT('',(-7.3,1.15470053837925,2.));
#66334=CARTESIAN_POINT('',(-7.3,2.3094010767585,1.33236321473148E-16));
#66335=CARTESIAN_POINT('',(-7.3,1.15470053837925,2.));
#66336=CARTESIAN_POINT('',(-7.3,-1.15470053837925,2.));
#66337=CARTESIAN_POINT('',(-7.3,-1.15470053837925,2.));
#66338=CARTESIAN_POINT('',(-7.3,-2.3094010767585,4.08864764769604E-16));
#66339=CARTESIAN_POINT('',(-7.3,-2.3094010767585,4.08864764769604E-16));
#66340=CARTESIAN_POINT('',(-7.3,-1.15470053837925,-2.));
#66341=CARTESIAN_POINT('',(-7.3,-1.15470053837925,-2.));
#66342=CARTESIAN_POINT('',(-7.3,1.15470053837925,-2.));
#66343=CARTESIAN_POINT('',(-7.3,1.15470053837925,-2.));
#66344=CARTESIAN_POINT('',(-7.3,2.3094010767585,1.33236321473148E-16));
#66345=CARTESIAN_POINT('Origin',(22.7,3.,0.));
#66346=CARTESIAN_POINT('Origin',(2.85,3.,0.));
#66347=CARTESIAN_POINT('Origin',(-2.3,2.065,0.));
#66348=CARTESIAN_POINT('Origin',(-4.8,-1.15470053837925,2.));
#66349=CARTESIAN_POINT('',(-4.8,-1.15470053837925,2.));
#66350=CARTESIAN_POINT('',(-4.8,-1.15470053837925,2.));
#66351=CARTESIAN_POINT('',(-4.8,-1.15470053837925,2.));
#66352=CARTESIAN_POINT('',(-4.8,1.15470053837925,2.));
#66353=CARTESIAN_POINT('',(-4.8,1.15470053837925,2.));
#66354=CARTESIAN_POINT('',(-4.8,-1.15470053837925,2.));
#66355=CARTESIAN_POINT('Origin',(-4.8,-2.3094010767585,4.08864764769604E-16));
#66356=CARTESIAN_POINT('',(-4.8,-2.3094010767585,4.08864764769604E-16));
#66357=CARTESIAN_POINT('',(-4.8,-2.3094010767585,4.08864764769604E-16));
#66358=CARTESIAN_POINT('',(-4.8,-2.3094010767585,4.08864764769604E-16));
#66359=CARTESIAN_POINT('',(-4.8,-2.3094010767585,4.08864764769604E-16));
#66360=CARTESIAN_POINT('Origin',(-4.8,-1.15470053837925,-2.));
#66361=CARTESIAN_POINT('',(-4.8,-1.15470053837925,-2.));
#66362=CARTESIAN_POINT('',(-4.8,-1.15470053837925,-2.));
#66363=CARTESIAN_POINT('',(-4.8,-1.15470053837925,-2.));
#66364=CARTESIAN_POINT('',(-4.8,-1.15470053837925,-2.));
#66365=CARTESIAN_POINT('Origin',(-4.8,1.15470053837925,-2.));
#66366=CARTESIAN_POINT('',(-4.8,1.15470053837925,-2.));
#66367=CARTESIAN_POINT('',(-4.8,1.15470053837925,-2.));
#66368=CARTESIAN_POINT('',(-4.8,1.15470053837925,-2.));
#66369=CARTESIAN_POINT('',(-4.8,1.15470053837925,-2.));
#66370=CARTESIAN_POINT('Origin',(-4.8,2.3094010767585,1.33236321473148E-16));
#66371=CARTESIAN_POINT('',(-4.8,2.3094010767585,1.33236321473148E-16));
#66372=CARTESIAN_POINT('',(-4.8,2.3094010767585,1.33236321473148E-16));
#66373=CARTESIAN_POINT('',(-4.8,2.3094010767585,1.33236321473148E-16));
#66374=CARTESIAN_POINT('',(-4.8,2.3094010767585,1.33236321473148E-16));
#66375=CARTESIAN_POINT('Origin',(-4.8,1.15470053837925,2.));
#66376=CARTESIAN_POINT('',(-4.8,1.15470053837925,2.));
#66377=CARTESIAN_POINT('',(-4.8,1.15470053837925,2.));
#66378=CARTESIAN_POINT('Origin',(-4.8,0.,0.));
#66379=CARTESIAN_POINT('Origin',(-4.8,0.,0.));
#66380=CARTESIAN_POINT('Origin',(-4.8,0.,0.));
#66381=CARTESIAN_POINT('Origin',(-4.8,0.,0.));
#66382=CARTESIAN_POINT('Origin',(-4.8,0.,0.));
#66383=CARTESIAN_POINT('Origin',(-4.8,0.,0.));
#66384=CARTESIAN_POINT('Origin',(-7.3,-2.80889253323697E-17,0.));
#66385=CARTESIAN_POINT('',(-1.,5.,-6.12323399573677E-16));
#66386=CARTESIAN_POINT('Origin',(-1.,-3.84779799073558E-18,0.));
#66387=CARTESIAN_POINT('',(0.,5.,-6.12323399573677E-16));
#66388=CARTESIAN_POINT('',(-7.3,5.,-6.12323399573677E-16));
#66389=CARTESIAN_POINT('Origin',(0.,0.,0.));
#66390=CARTESIAN_POINT('Origin',(-7.3,-2.80889253323697E-17,0.));
#66391=CARTESIAN_POINT('',(0.,2.5,-3.06161699786838E-16));
#66392=CARTESIAN_POINT('Origin',(0.,0.,0.));
#66393=CARTESIAN_POINT('',(-1.,2.5,-3.06161699786838E-16));
#66394=CARTESIAN_POINT('',(-7.3,2.5,-3.06161699786838E-16));
#66395=CARTESIAN_POINT('Origin',(-1.,-3.84779799073558E-18,0.));
#66396=CARTESIAN_POINT('Origin',(-1.,5.,0.));
#66397=CARTESIAN_POINT('Origin',(-3.54259174671033E-17,5.,0.));
#66398=CARTESIAN_POINT('Origin',(-2.3,-2.80889253323697E-17,0.));
#66399=CARTESIAN_POINT('',(-1.,1.065,4.11439849795812));
#66400=CARTESIAN_POINT('',(-1.,-1.065,4.11439849795812));
#66401=CARTESIAN_POINT('Origin',(-1.,-1.22125762314651E-17,0.));
#66402=CARTESIAN_POINT('',(-2.3,-1.065,4.11439849795812));
#66403=CARTESIAN_POINT('',(-2.3,-1.065,4.11439849795812));
#66404=CARTESIAN_POINT('',(-2.3,1.065,4.11439849795812));
#66405=CARTESIAN_POINT('Origin',(-2.3,-2.80889253323697E-17,0.));
#66406=CARTESIAN_POINT('',(-2.3,1.065,4.11439849795812));
#66407=CARTESIAN_POINT('Origin',(-2.3,-2.80889253323697E-17,0.));
#66408=CARTESIAN_POINT('',(-1.,1.065,2.26180790519443));
#66409=CARTESIAN_POINT('',(-1.,-1.065,2.26180790519443));
#66410=CARTESIAN_POINT('Origin',(-1.,-1.22125762314651E-17,0.));
#66411=CARTESIAN_POINT('',(-2.3,1.065,2.26180790519443));
#66412=CARTESIAN_POINT('',(-2.3,1.065,2.26180790519443));
#66413=CARTESIAN_POINT('',(-2.3,-1.065,2.26180790519443));
#66414=CARTESIAN_POINT('Origin',(-2.3,-2.80889253323697E-17,0.));
#66415=CARTESIAN_POINT('',(-2.3,-1.065,2.26180790519443));
#66416=CARTESIAN_POINT('Origin',(-2.3,4.25,0.));
#66417=CARTESIAN_POINT('',(-2.3,-1.065,4.11439849795812));
#66418=CARTESIAN_POINT('',(-2.3,1.065,4.11439849795812));
#66419=CARTESIAN_POINT('Origin',(-1.,4.25,0.));
#66420=CARTESIAN_POINT('',(-1.,-1.065,4.11439849795812));
#66421=CARTESIAN_POINT('',(-1.,1.065,4.11439849795812));
#66422=CARTESIAN_POINT('Origin',(-2.3,1.065,4.11439849795812));
#66423=CARTESIAN_POINT('Origin',(-2.3,-1.065,4.11439849795812));
#66677=UNCERTAINTY_MEASURE_WITH_UNIT(LENGTH_MEASURE(0.01),#66722,
'DISTANCE_ACCURACY_VALUE',
'Maximum model space distance between geometric entities at asserted c
onnectivities');
#66680=UNCERTAINTY_MEASURE_WITH_UNIT(LENGTH_MEASURE(0.01),#66722,
'DISTANCE_ACCURACY_VALUE',
'Maximum model space distance between geometric entities at asserted c
onnectivities');
#66718=(
GEOMETRIC_REPRESENTATION_CONTEXT(3)
GLOBAL_UNCERTAINTY_ASSIGNED_CONTEXT((#66677))
GLOBAL_UNIT_ASSIGNED_CONTEXT((#66722,#66724,#66725))
REPRESENTATION_CONTEXT('','3D')
);
#66721=(
GEOMETRIC_REPRESENTATION_CONTEXT(3)
GLOBAL_UNCERTAINTY_ASSIGNED_CONTEXT((#66680))
GLOBAL_UNIT_ASSIGNED_CONTEXT((#66722,#66724,#66725))
REPRESENTATION_CONTEXT('','3D')
);
#66722=(
LENGTH_UNIT()
NAMED_UNIT(*)
SI_UNIT(.MILLI.,.METRE.)
);
#66724=(
NAMED_UNIT(*)
PLANE_ANGLE_UNIT()
SI_UNIT($,.RADIAN.)
);
#66725=(
NAMED_UNIT(*)
SI_UNIT($,.STERADIAN.)
SOLID_ANGLE_UNIT()
);
#66763=SHAPE_DEFINITION_REPRESENTATION(#66833,#66927);
#66833=PRODUCT_DEFINITION_SHAPE('',$,#66968);
#66927=SHAPE_REPRESENTATION('',(#28586),#66718);
#66930=PRODUCT_DEFINITION_CONTEXT('part definition',#67052,'design');
#66968=PRODUCT_DEFINITION('Low Head Cap Screw M6x25',
'Low Head Cap Screw M6x25',#67008,#66930);
#67008=PRODUCT_DEFINITION_FORMATION('',$,#67091);
#67052=APPLICATION_CONTEXT(
'Core Data for Automotive Mechanical Design Process');
#67053=PRODUCT_CONTEXT('part definition',#67052,'mechanical');
#67091=PRODUCT('Low Head Cap Screw M6x25','Low Head Cap Screw M6x25',$,
(#67053));
#67095=PRESENTATION_STYLE_ASSIGNMENT((#67097));
#67097=SURFACE_STYLE_USAGE(.BOTH.,#67099);
#67099=SURFACE_SIDE_STYLE('',(#67101));
#67101=SURFACE_STYLE_FILL_AREA(#67103);
#67103=FILL_AREA_STYLE('Opaque(202,209,238)',(#67105));
#67105=FILL_AREA_STYLE_COLOUR('Opaque(202,209,238)',#67107);
#67107=COLOUR_RGB('Opaque(202,209,238)',0.792156862745098,0.819607843137255,
0.933333333333333);
ENDSEC;
END-ISO-10303-21;
